ISO-10303-21;
HEADER;
/* Generated by software containing ST-Developer
 * from STEP Tools, Inc. (www.steptools.com) 
 */

FILE_DESCRIPTION(
/* description */ (''),
/* implementation_level */ '2;1');

FILE_NAME(
/* name */ 'Nut.step',
/* time_stamp */ '2026-10-04T16:36:43-07:00',
/* author */ (''),
/* organization */ (''),
/* preprocessor_version */ 'ST-DEVELOPER v20.2',
/* originating_system */ 'Autodesk Translation Framework v15.15.0.0',
/* authorisation */ '');

FILE_SCHEMA (('AUTOMOTIVE_DESIGN { 1 0 10303 214 3 1 1 }'));
ENDSEC;

DATA;
#10=MECHANICAL_DESIGN_GEOMETRIC_PRESENTATION_REPRESENTATION('',(#71),#33474);
#33=(
BOUNDED_CURVE()
B_SPLINE_CURVE(2,(#33377,#33378,#33379),.UNSPECIFIED.,.F.,.F.)
B_SPLINE_CURVE_WITH_KNOTS((3,3),(0.000182870967167632,0.407532766922341),
 .UNSPECIFIED.)
CURVE()
GEOMETRIC_REPRESENTATION_ITEM()
RATIONAL_B_SPLINE_CURVE((1.00013898062186,1.15486101937814,1.00013898062186))
REPRESENTATION_ITEM('')
);
#34=(
BOUNDED_CURVE()
B_SPLINE_CURVE(2,(#33382,#33383,#33384),.UNSPECIFIED.,.F.,.F.)
B_SPLINE_CURVE_WITH_KNOTS((3,3),(0.000182870967168132,0.407532766922342),
 .UNSPECIFIED.)
CURVE()
GEOMETRIC_REPRESENTATION_ITEM()
RATIONAL_B_SPLINE_CURVE((1.00013898062186,1.15486101937814,1.00013898062186))
REPRESENTATION_ITEM('')
);
#35=(
BOUNDED_CURVE()
B_SPLINE_CURVE(2,(#33387,#33388,#33389),.UNSPECIFIED.,.F.,.F.)
B_SPLINE_CURVE_WITH_KNOTS((3,3),(0.000182870967167337,0.407532766922341),
 .UNSPECIFIED.)
CURVE()
GEOMETRIC_REPRESENTATION_ITEM()
RATIONAL_B_SPLINE_CURVE((1.00013898062186,1.15486101937814,1.00013898062186))
REPRESENTATION_ITEM('')
);
#36=(
BOUNDED_CURVE()
B_SPLINE_CURVE(2,(#33392,#33393,#33394),.UNSPECIFIED.,.F.,.F.)
B_SPLINE_CURVE_WITH_KNOTS((3,3),(0.000182870967167613,0.407532766922341),
 .UNSPECIFIED.)
CURVE()
GEOMETRIC_REPRESENTATION_ITEM()
RATIONAL_B_SPLINE_CURVE((1.00013898062186,1.15486101937814,1.00013898062186))
REPRESENTATION_ITEM('')
);
#37=(
BOUNDED_CURVE()
B_SPLINE_CURVE(2,(#33401,#33402,#33403),.UNSPECIFIED.,.F.,.F.)
B_SPLINE_CURVE_WITH_KNOTS((3,3),(0.203857818944754,0.407532766922341),
 .UNSPECIFIED.)
CURVE()
GEOMETRIC_REPRESENTATION_ITEM()
RATIONAL_B_SPLINE_CURVE((1.0775,1.0775,1.00013898062186))
REPRESENTATION_ITEM('')
);
#38=(
BOUNDED_CURVE()
B_SPLINE_CURVE(2,(#33405,#33406,#33407),.UNSPECIFIED.,.F.,.F.)
B_SPLINE_CURVE_WITH_KNOTS((3,3),(0.000182870967167808,0.407532766922341),
 .UNSPECIFIED.)
CURVE()
GEOMETRIC_REPRESENTATION_ITEM()
RATIONAL_B_SPLINE_CURVE((1.00013898062186,1.15486101937814,1.00013898062186))
REPRESENTATION_ITEM('')
);
#39=(
BOUNDED_CURVE()
B_SPLINE_CURVE(2,(#33408,#33409,#33410),.UNSPECIFIED.,.F.,.F.)
B_SPLINE_CURVE_WITH_KNOTS((3,3),(0.000182870967168059,0.407532766922341),
 .UNSPECIFIED.)
CURVE()
GEOMETRIC_REPRESENTATION_ITEM()
RATIONAL_B_SPLINE_CURVE((1.00013898062186,1.15486101937814,1.00013898062186))
REPRESENTATION_ITEM('')
);
#40=(
BOUNDED_CURVE()
B_SPLINE_CURVE(2,(#33412,#33413,#33414),.UNSPECIFIED.,.F.,.F.)
B_SPLINE_CURVE_WITH_KNOTS((3,3),(0.000182870967167986,0.407532766922341),
 .UNSPECIFIED.)
CURVE()
GEOMETRIC_REPRESENTATION_ITEM()
RATIONAL_B_SPLINE_CURVE((1.00013898062186,1.15486101937814,1.00013898062186))
REPRESENTATION_ITEM('')
);
#41=(
BOUNDED_CURVE()
B_SPLINE_CURVE(2,(#33415,#33416,#33417),.UNSPECIFIED.,.F.,.F.)
B_SPLINE_CURVE_WITH_KNOTS((3,3),(0.000182870967167794,0.203857818944754),
 .UNSPECIFIED.)
CURVE()
GEOMETRIC_REPRESENTATION_ITEM()
RATIONAL_B_SPLINE_CURVE((1.00013898062186,1.0775,1.0775))
REPRESENTATION_ITEM('')
);
#42=(
BOUNDED_CURVE()
B_SPLINE_CURVE(2,(#33420,#33421,#33422),.UNSPECIFIED.,.F.,.F.)
B_SPLINE_CURVE_WITH_KNOTS((3,3),(0.000182870967168019,0.407532766922341),
 .UNSPECIFIED.)
CURVE()
GEOMETRIC_REPRESENTATION_ITEM()
RATIONAL_B_SPLINE_CURVE((1.00013898062186,1.15486101937814,1.00013898062186))
REPRESENTATION_ITEM('')
);
#43=(
BOUNDED_CURVE()
B_SPLINE_CURVE(2,(#33426,#33427,#33428),.UNSPECIFIED.,.F.,.F.)
B_SPLINE_CURVE_WITH_KNOTS((3,3),(0.203857818944755,0.407532766922341),
 .UNSPECIFIED.)
CURVE()
GEOMETRIC_REPRESENTATION_ITEM()
RATIONAL_B_SPLINE_CURVE((1.0775,1.0775,1.00013898062186))
REPRESENTATION_ITEM('')
);
#44=(
BOUNDED_CURVE()
B_SPLINE_CURVE(2,(#33430,#33431,#33432),.UNSPECIFIED.,.F.,.F.)
B_SPLINE_CURVE_WITH_KNOTS((3,3),(0.000182870967167917,0.203857818944755),
 .UNSPECIFIED.)
CURVE()
GEOMETRIC_REPRESENTATION_ITEM()
RATIONAL_B_SPLINE_CURVE((1.00013898062186,1.0775,1.0775))
REPRESENTATION_ITEM('')
);
#45=(
BOUNDED_CURVE()
B_SPLINE_CURVE(2,(#33436,#33437,#33438),.UNSPECIFIED.,.F.,.F.)
B_SPLINE_CURVE_WITH_KNOTS((3,3),(0.000182870967168095,0.407532766922342),
 .UNSPECIFIED.)
CURVE()
GEOMETRIC_REPRESENTATION_ITEM()
RATIONAL_B_SPLINE_CURVE((1.00013898062186,1.15486101937814,1.00013898062186))
REPRESENTATION_ITEM('')
);
#46=(
BOUNDED_CURVE()
B_SPLINE_CURVE(2,(#33441,#33442,#33443),.UNSPECIFIED.,.F.,.F.)
B_SPLINE_CURVE_WITH_KNOTS((3,3),(0.000182870967167807,0.407532766922341),
 .UNSPECIFIED.)
CURVE()
GEOMETRIC_REPRESENTATION_ITEM()
RATIONAL_B_SPLINE_CURVE((1.00013898062186,1.15486101937814,1.00013898062186))
REPRESENTATION_ITEM('')
);
#55=CONICAL_SURFACE('',#3131,3.73625,1.13446401379631);
#56=CONICAL_SURFACE('',#3140,3.73625,1.13446401379632);
#61=SHAPE_REPRESENTATION_RELATIONSHIP('SRR','None',#33501,#66);
#66=ADVANCED_BREP_SHAPE_REPRESENTATION('',(#76),#33473);
#71=STYLED_ITEM('',(#33530),#76);
#76=MANIFOLD_SOLID_BREP('Body1',#2811);
#89=FACE_BOUND('',#540,.T.);
#90=FACE_BOUND('',#543,.T.);
#97=PLANE('',#3129);
#98=PLANE('',#3130);
#99=PLANE('',#3133);
#100=PLANE('',#3134);
#101=PLANE('',#3135);
#102=PLANE('',#3136);
#103=PLANE('',#3137);
#104=PLANE('',#3141);
#193=LINE('',#33375,#290);
#194=LINE('',#33381,#291);
#195=LINE('',#33391,#292);
#196=LINE('',#33399,#293);
#197=LINE('',#33423,#294);
#198=LINE('',#33433,#295);
#199=LINE('',#33439,#296);
#200=LINE('',#33450,#297);
#201=LINE('',#33455,#298);
#290=VECTOR('',#3761,10.);
#291=VECTOR('',#3762,10.);
#292=VECTOR('',#3765,10.);
#293=VECTOR('',#3770,3.73625);
#294=VECTOR('',#3773,10.);
#295=VECTOR('',#3776,10.);
#296=VECTOR('',#3779,10.);
#297=VECTOR('',#3790,3.73625);
#298=VECTOR('',#3797,2.);
#409=FACE_OUTER_BOUND('',#532,.T.);
#410=FACE_OUTER_BOUND('',#533,.T.);
#411=FACE_OUTER_BOUND('',#534,.T.);
#412=FACE_OUTER_BOUND('',#535,.T.);
#413=FACE_OUTER_BOUND('',#536,.T.);
#414=FACE_OUTER_BOUND('',#537,.T.);
#415=FACE_OUTER_BOUND('',#538,.T.);
#416=FACE_OUTER_BOUND('',#539,.T.);
#417=FACE_OUTER_BOUND('',#541,.T.);
#418=FACE_OUTER_BOUND('',#542,.T.);
#419=FACE_OUTER_BOUND('',#544,.T.);
#532=EDGE_LOOP('',(#2545,#2546,#2547,#2548));
#533=EDGE_LOOP('',(#2549,#2550,#2551,#2552));
#534=EDGE_LOOP('',(#2553,#2554,#2555,#2556,#2557,#2558,#2559,#2560,#2561,
#2562));
#535=EDGE_LOOP('',(#2563,#2564,#2565,#2566));
#536=EDGE_LOOP('',(#2567,#2568,#2569,#2570,#2571,#2572));
#537=EDGE_LOOP('',(#2573,#2574,#2575,#2576));
#538=EDGE_LOOP('',(#2577,#2578,#2579,#2580));
#539=EDGE_LOOP('',(#2581));
#540=EDGE_LOOP('',(#2582));
#541=EDGE_LOOP('',(#2583,#2584,#2585,#2586,#2587,#2588,#2589,#2590,#2591,
#2592));
#542=EDGE_LOOP('',(#2593));
#543=EDGE_LOOP('',(#2594));
#544=EDGE_LOOP('',(#2595,#2596,#2597,#2598));
#697=CIRCLE('',#3132,3.43);
#698=CIRCLE('',#3138,3.43);
#699=CIRCLE('',#3139,1.666);
#700=CIRCLE('',#3142,1.666);
#1213=VERTEX_POINT('',#33373);
#1214=VERTEX_POINT('',#33374);
#1215=VERTEX_POINT('',#33376);
#1216=VERTEX_POINT('',#33380);
#1217=VERTEX_POINT('',#33386);
#1218=VERTEX_POINT('',#33390);
#1219=VERTEX_POINT('',#33396);
#1220=VERTEX_POINT('',#33398);
#1221=VERTEX_POINT('',#33400);
#1222=VERTEX_POINT('',#33404);
#1223=VERTEX_POINT('',#33411);
#1224=VERTEX_POINT('',#33419);
#1225=VERTEX_POINT('',#33425);
#1226=VERTEX_POINT('',#33429);
#1227=VERTEX_POINT('',#33435);
#1228=VERTEX_POINT('',#33445);
#1229=VERTEX_POINT('',#33447);
#1230=VERTEX_POINT('',#33452);
#1660=EDGE_CURVE('',#1213,#1214,#193,.T.);
#1661=EDGE_CURVE('',#1215,#1213,#33,.T.);
#1662=EDGE_CURVE('',#1216,#1215,#194,.T.);
#1663=EDGE_CURVE('',#1214,#1216,#34,.T.);
#1664=EDGE_CURVE('',#1217,#1215,#35,.T.);
#1665=EDGE_CURVE('',#1217,#1218,#195,.T.);
#1666=EDGE_CURVE('',#1216,#1218,#36,.T.);
#1667=EDGE_CURVE('',#1219,#1219,#697,.T.);
#1668=EDGE_CURVE('',#1219,#1220,#196,.T.);
#1669=EDGE_CURVE('',#1220,#1221,#37,.T.);
#1670=EDGE_CURVE('',#1221,#1222,#38,.T.);
#1671=EDGE_CURVE('',#1222,#1217,#39,.T.);
#1672=EDGE_CURVE('',#1213,#1223,#40,.T.);
#1673=EDGE_CURVE('',#1223,#1220,#41,.T.);
#1674=EDGE_CURVE('',#1224,#1214,#42,.T.);
#1675=EDGE_CURVE('',#1223,#1224,#197,.T.);
#1676=EDGE_CURVE('',#1225,#1224,#43,.T.);
#1677=EDGE_CURVE('',#1226,#1225,#44,.T.);
#1678=EDGE_CURVE('',#1221,#1226,#198,.T.);
#1679=EDGE_CURVE('',#1227,#1226,#45,.T.);
#1680=EDGE_CURVE('',#1222,#1227,#199,.T.);
#1681=EDGE_CURVE('',#1218,#1227,#46,.T.);
#1682=EDGE_CURVE('',#1228,#1228,#698,.T.);
#1683=EDGE_CURVE('',#1229,#1229,#699,.F.);
#1684=EDGE_CURVE('',#1225,#1228,#200,.T.);
#1685=EDGE_CURVE('',#1230,#1230,#700,.T.);
#1686=EDGE_CURVE('',#1230,#1229,#201,.T.);
#2545=ORIENTED_EDGE('',*,*,#1660,.F.);
#2546=ORIENTED_EDGE('',*,*,#1661,.F.);
#2547=ORIENTED_EDGE('',*,*,#1662,.F.);
#2548=ORIENTED_EDGE('',*,*,#1663,.F.);
#2549=ORIENTED_EDGE('',*,*,#1662,.T.);
#2550=ORIENTED_EDGE('',*,*,#1664,.F.);
#2551=ORIENTED_EDGE('',*,*,#1665,.T.);
#2552=ORIENTED_EDGE('',*,*,#1666,.F.);
#2553=ORIENTED_EDGE('',*,*,#1667,.F.);
#2554=ORIENTED_EDGE('',*,*,#1668,.T.);
#2555=ORIENTED_EDGE('',*,*,#1669,.T.);
#2556=ORIENTED_EDGE('',*,*,#1670,.T.);
#2557=ORIENTED_EDGE('',*,*,#1671,.T.);
#2558=ORIENTED_EDGE('',*,*,#1664,.T.);
#2559=ORIENTED_EDGE('',*,*,#1661,.T.);
#2560=ORIENTED_EDGE('',*,*,#1672,.T.);
#2561=ORIENTED_EDGE('',*,*,#1673,.T.);
#2562=ORIENTED_EDGE('',*,*,#1668,.F.);
#2563=ORIENTED_EDGE('',*,*,#1660,.T.);
#2564=ORIENTED_EDGE('',*,*,#1674,.F.);
#2565=ORIENTED_EDGE('',*,*,#1675,.F.);
#2566=ORIENTED_EDGE('',*,*,#1672,.F.);
#2567=ORIENTED_EDGE('',*,*,#1675,.T.);
#2568=ORIENTED_EDGE('',*,*,#1676,.F.);
#2569=ORIENTED_EDGE('',*,*,#1677,.F.);
#2570=ORIENTED_EDGE('',*,*,#1678,.F.);
#2571=ORIENTED_EDGE('',*,*,#1669,.F.);
#2572=ORIENTED_EDGE('',*,*,#1673,.F.);
#2573=ORIENTED_EDGE('',*,*,#1678,.T.);
#2574=ORIENTED_EDGE('',*,*,#1679,.F.);
#2575=ORIENTED_EDGE('',*,*,#1680,.F.);
#2576=ORIENTED_EDGE('',*,*,#1670,.F.);
#2577=ORIENTED_EDGE('',*,*,#1680,.T.);
#2578=ORIENTED_EDGE('',*,*,#1681,.F.);
#2579=ORIENTED_EDGE('',*,*,#1665,.F.);
#2580=ORIENTED_EDGE('',*,*,#1671,.F.);
#2581=ORIENTED_EDGE('',*,*,#1682,.F.);
#2582=ORIENTED_EDGE('',*,*,#1683,.T.);
#2583=ORIENTED_EDGE('',*,*,#1663,.T.);
#2584=ORIENTED_EDGE('',*,*,#1666,.T.);
#2585=ORIENTED_EDGE('',*,*,#1681,.T.);
#2586=ORIENTED_EDGE('',*,*,#1679,.T.);
#2587=ORIENTED_EDGE('',*,*,#1677,.T.);
#2588=ORIENTED_EDGE('',*,*,#1684,.T.);
#2589=ORIENTED_EDGE('',*,*,#1682,.T.);
#2590=ORIENTED_EDGE('',*,*,#1684,.F.);
#2591=ORIENTED_EDGE('',*,*,#1676,.T.);
#2592=ORIENTED_EDGE('',*,*,#1674,.T.);
#2593=ORIENTED_EDGE('',*,*,#1667,.T.);
#2594=ORIENTED_EDGE('',*,*,#1685,.F.);
#2595=ORIENTED_EDGE('',*,*,#1685,.T.);
#2596=ORIENTED_EDGE('',*,*,#1686,.T.);
#2597=ORIENTED_EDGE('',*,*,#1683,.F.);
#2598=ORIENTED_EDGE('',*,*,#1686,.F.);
#2685=CYLINDRICAL_SURFACE('',#3143,1.666);
#2796=ADVANCED_FACE('',(#409),#97,.F.);
#2797=ADVANCED_FACE('',(#410),#98,.F.);
#2798=ADVANCED_FACE('',(#411),#55,.T.);
#2799=ADVANCED_FACE('',(#412),#99,.F.);
#2800=ADVANCED_FACE('',(#413),#100,.F.);
#2801=ADVANCED_FACE('',(#414),#101,.F.);
#2802=ADVANCED_FACE('',(#415),#102,.F.);
#2803=ADVANCED_FACE('',(#416,#89),#103,.T.);
#2804=ADVANCED_FACE('',(#417),#56,.T.);
#2805=ADVANCED_FACE('',(#418,#90),#104,.T.);
#2806=ADVANCED_FACE('',(#419),#2685,.F.);
#2811=CLOSED_SHELL('',(#2796,#2797,#2798,#2799,#2800,#2801,#2802,#2803,
#2804,#2805,#2806));
#3128=AXIS2_PLACEMENT_3D('',#33371,#3757,#3758);
#3129=AXIS2_PLACEMENT_3D('',#33372,#3759,#3760);
#3130=AXIS2_PLACEMENT_3D('',#33385,#3763,#3764);
#3131=AXIS2_PLACEMENT_3D('',#33395,#3766,#3767);
#3132=AXIS2_PLACEMENT_3D('',#33397,#3768,#3769);
#3133=AXIS2_PLACEMENT_3D('',#33418,#3771,#3772);
#3134=AXIS2_PLACEMENT_3D('',#33424,#3774,#3775);
#3135=AXIS2_PLACEMENT_3D('',#33434,#3777,#3778);
#3136=AXIS2_PLACEMENT_3D('',#33440,#3780,#3781);
#3137=AXIS2_PLACEMENT_3D('',#33444,#3782,#3783);
#3138=AXIS2_PLACEMENT_3D('',#33446,#3784,#3785);
#3139=AXIS2_PLACEMENT_3D('',#33448,#3786,#3787);
#3140=AXIS2_PLACEMENT_3D('',#33449,#3788,#3789);
#3141=AXIS2_PLACEMENT_3D('',#33451,#3791,#3792);
#3142=AXIS2_PLACEMENT_3D('',#33453,#3793,#3794);
#3143=AXIS2_PLACEMENT_3D('',#33454,#3795,#3796);
#3757=DIRECTION('axis',(0.,0.,1.));
#3758=DIRECTION('refdir',(1.,0.,0.));
#3759=DIRECTION('center_axis',(0.499999999999999,-0.866025403784439,0.));
#3760=DIRECTION('ref_axis',(-0.866025403784439,-0.499999999999999,0.));
#3761=DIRECTION('',(0.,0.,1.));
#3762=DIRECTION('',(0.,0.,-1.));
#3763=DIRECTION('center_axis',(1.,-6.86060968596774E-16,0.));
#3764=DIRECTION('ref_axis',(-6.86060968596774E-16,-1.,0.));
#3765=DIRECTION('',(0.,0.,1.));
#3766=DIRECTION('center_axis',(0.,0.,1.));
#3767=DIRECTION('ref_axis',(-1.,0.,0.));
#3768=DIRECTION('center_axis',(0.,0.,-1.));
#3769=DIRECTION('ref_axis',(1.,0.,0.));
#3770=DIRECTION('',(0.90630778703665,-1.10990693043675E-16,0.4226182617407));
#3771=DIRECTION('center_axis',(-0.500000000000001,-0.866025403784438,0.));
#3772=DIRECTION('ref_axis',(-0.866025403784438,0.500000000000001,0.));
#3773=DIRECTION('',(0.,0.,1.));
#3774=DIRECTION('center_axis',(-1.,8.0852564851151E-16,0.));
#3775=DIRECTION('ref_axis',(8.0852564851151E-16,1.,0.));
#3776=DIRECTION('',(0.,0.,1.));
#3777=DIRECTION('center_axis',(-0.499999999999999,0.866025403784439,0.));
#3778=DIRECTION('ref_axis',(0.866025403784439,0.499999999999999,0.));
#3779=DIRECTION('',(0.,0.,1.));
#3780=DIRECTION('center_axis',(0.500000000000001,0.866025403784438,0.));
#3781=DIRECTION('ref_axis',(0.866025403784438,-0.500000000000001,0.));
#3782=DIRECTION('center_axis',(0.,0.,1.));
#3783=DIRECTION('ref_axis',(1.,0.,0.));
#3784=DIRECTION('center_axis',(0.,0.,-1.));
#3785=DIRECTION('ref_axis',(1.,0.,0.));
#3786=DIRECTION('center_axis',(0.,0.,1.));
#3787=DIRECTION('ref_axis',(-1.,0.,0.));
#3788=DIRECTION('center_axis',(0.,0.,-1.));
#3789=DIRECTION('ref_axis',(-1.,0.,0.));
#3790=DIRECTION('',(-0.906307787036652,1.10990693043676E-16,0.422618261740694));
#3791=DIRECTION('center_axis',(0.,0.,-1.));
#3792=DIRECTION('ref_axis',(-1.,0.,0.));
#3793=DIRECTION('center_axis',(0.,0.,-1.));
#3794=DIRECTION('ref_axis',(-1.,0.,0.));
#3795=DIRECTION('center_axis',(0.,0.,-1.));
#3796=DIRECTION('ref_axis',(-1.,0.,0.));
#3797=DIRECTION('',(0.,0.,1.));
#33371=CARTESIAN_POINT('',(0.,0.,0.));
#33372=CARTESIAN_POINT('Origin',(0.00181468412045555,4.04249959269282,3.2));
#33373=CARTESIAN_POINT('',(5.58144376948235E-15,4.04145188432738,0.285124696255161));
#33374=CARTESIAN_POINT('',(5.95743279803446E-15,4.04145188432738,2.91487530374485));
#33375=CARTESIAN_POINT('',(5.55111512312578E-15,4.04145188432738,3.2));
#33376=CARTESIAN_POINT('',(-3.5,2.02072594216369,0.285124696255161));
#33377=CARTESIAN_POINT('Ctrl Pts',(-3.5,2.02072594216369,0.285124696255161));
#33378=CARTESIAN_POINT('Ctrl Pts',(-1.75,3.03108891324554,-0.186015294676542));
#33379=CARTESIAN_POINT('Ctrl Pts',(5.58144376948235E-15,4.04145188432738,
0.285124696255161));
#33380=CARTESIAN_POINT('',(-3.5,2.02072594216369,2.91487530374484));
#33381=CARTESIAN_POINT('',(-3.5,2.02072594216369,3.2));
#33382=CARTESIAN_POINT('Ctrl Pts',(5.95743279803446E-15,4.04145188432738,
2.91487530374485));
#33383=CARTESIAN_POINT('Ctrl Pts',(-1.75,3.03108891324554,3.38601529467654));
#33384=CARTESIAN_POINT('Ctrl Pts',(-3.5,2.02072594216369,2.91487530374484));
#33385=CARTESIAN_POINT('Origin',(-3.5,2.02282135889456,3.2));
#33386=CARTESIAN_POINT('',(-3.5,-2.02072594216369,0.285124696255161));
#33387=CARTESIAN_POINT('Ctrl Pts',(-3.5,-2.02072594216369,0.285124696255161));
#33388=CARTESIAN_POINT('Ctrl Pts',(-3.5,3.05311331771918E-15,-0.186015294676541));
#33389=CARTESIAN_POINT('Ctrl Pts',(-3.5,2.02072594216369,0.285124696255161));
#33390=CARTESIAN_POINT('',(-3.5,-2.02072594216369,2.91487530374484));
#33391=CARTESIAN_POINT('',(-3.5,-2.02072594216369,3.2));
#33392=CARTESIAN_POINT('Ctrl Pts',(-3.5,2.02072594216369,2.91487530374484));
#33393=CARTESIAN_POINT('Ctrl Pts',(-3.5,3.60822483003176E-15,3.38601529467654));
#33394=CARTESIAN_POINT('Ctrl Pts',(-3.5,-2.02072594216369,2.91487530374484));
#33395=CARTESIAN_POINT('Origin',(0.,0.,0.142806720309968));
#33396=CARTESIAN_POINT('',(3.43,-4.20053852107542E-16,-5.20417042793042E-16));
#33397=CARTESIAN_POINT('Origin',(0.,0.,-2.77555756156289E-16));
#33398=CARTESIAN_POINT('',(3.5,-4.0750745167651E-16,0.032641536070849));
#33399=CARTESIAN_POINT('',(3.73625,-4.5755866033143E-16,0.142806720309968));
#33400=CARTESIAN_POINT('',(3.5,-2.02072594216369,0.285124696255161));
#33401=CARTESIAN_POINT('Ctrl Pts',(3.5,-3.86388523651447E-16,0.032641536070849));
#33402=CARTESIAN_POINT('Ctrl Pts',(3.5,-0.937822173508931,0.0326415360708487));
#33403=CARTESIAN_POINT('Ctrl Pts',(3.5,-2.02072594216369,0.285124696255161));
#33404=CARTESIAN_POINT('',(-3.69459687690438E-15,-4.04145188432738,0.285124696255161));
#33405=CARTESIAN_POINT('Ctrl Pts',(3.5,-2.02072594216369,0.285124696255161));
#33406=CARTESIAN_POINT('Ctrl Pts',(1.75,-3.03108891324554,-0.186015294676541));
#33407=CARTESIAN_POINT('Ctrl Pts',(-3.69459687690438E-15,-4.04145188432738,
0.285124696255161));
#33408=CARTESIAN_POINT('Ctrl Pts',(-3.59512132757884E-15,-4.04145188432738,
0.285124696255161));
#33409=CARTESIAN_POINT('Ctrl Pts',(-1.75000000000001,-3.03108891324553,
-0.186015294676541));
#33410=CARTESIAN_POINT('Ctrl Pts',(-3.5,-2.02072594216369,0.285124696255161));
#33411=CARTESIAN_POINT('',(3.5,2.02072594216369,0.285124696255161));
#33412=CARTESIAN_POINT('Ctrl Pts',(5.57202476310889E-15,4.04145188432738,
0.285124696255161));
#33413=CARTESIAN_POINT('Ctrl Pts',(1.75,3.03108891324553,-0.186015294676541));
#33414=CARTESIAN_POINT('Ctrl Pts',(3.5,2.02072594216369,0.285124696255161));
#33415=CARTESIAN_POINT('Ctrl Pts',(3.5,2.02072594216369,0.285124696255161));
#33416=CARTESIAN_POINT('Ctrl Pts',(3.5,0.937822173508927,0.0326415360708494));
#33417=CARTESIAN_POINT('Ctrl Pts',(3.5,-3.86388523651447E-16,0.032641536070849));
#33418=CARTESIAN_POINT('Origin',(3.50181468412045,2.01967823379825,3.2));
#33419=CARTESIAN_POINT('',(3.5,2.02072594216369,2.91487530374484));
#33420=CARTESIAN_POINT('Ctrl Pts',(3.5,2.02072594216369,2.91487530374484));
#33421=CARTESIAN_POINT('Ctrl Pts',(1.75,3.03108891324553,3.38601529467654));
#33422=CARTESIAN_POINT('Ctrl Pts',(6.00171568051692E-15,4.04145188432738,
2.91487530374485));
#33423=CARTESIAN_POINT('',(3.5,2.02072594216369,3.2));
#33424=CARTESIAN_POINT('Origin',(3.5,-2.02282135889456,3.2));
#33425=CARTESIAN_POINT('',(3.5,-3.75308408038889E-16,3.16735846392915));
#33426=CARTESIAN_POINT('Ctrl Pts',(3.5,-3.21990436376205E-16,3.16735846392915));
#33427=CARTESIAN_POINT('Ctrl Pts',(3.5,0.937822173508926,3.16735846392915));
#33428=CARTESIAN_POINT('Ctrl Pts',(3.5,2.02072594216369,2.91487530374484));
#33429=CARTESIAN_POINT('',(3.5,-2.02072594216369,2.91487530374485));
#33430=CARTESIAN_POINT('Ctrl Pts',(3.5,-2.02072594216369,2.91487530374485));
#33431=CARTESIAN_POINT('Ctrl Pts',(3.5,-0.937822173508929,3.16735846392915));
#33432=CARTESIAN_POINT('Ctrl Pts',(3.5,-3.21990436376205E-16,3.16735846392915));
#33433=CARTESIAN_POINT('',(3.5,-2.02072594216369,3.2));
#33434=CARTESIAN_POINT('Origin',(-0.00181468412045332,-4.04249959269282,
3.2));
#33435=CARTESIAN_POINT('',(-3.93275951036187E-15,-4.04145188432738,2.91487530374484));
#33436=CARTESIAN_POINT('Ctrl Pts',(-3.93275951036187E-15,-4.04145188432738,
2.91487530374484));
#33437=CARTESIAN_POINT('Ctrl Pts',(1.75,-3.03108891324553,3.38601529467654));
#33438=CARTESIAN_POINT('Ctrl Pts',(3.5,-2.02072594216369,2.91487530374485));
#33439=CARTESIAN_POINT('',(-3.33066907387547E-15,-4.04145188432738,3.2));
#33440=CARTESIAN_POINT('Origin',(-3.50181468412045,-2.01967823379825,3.2));
#33441=CARTESIAN_POINT('Ctrl Pts',(-3.5,-2.02072594216369,2.91487530374484));
#33442=CARTESIAN_POINT('Ctrl Pts',(-1.75,-3.03108891324553,3.38601529467654));
#33443=CARTESIAN_POINT('Ctrl Pts',(-4.00462178560693E-15,-4.04145188432738,
2.91487530374484));
#33444=CARTESIAN_POINT('Origin',(-3.43,0.,3.2));
#33445=CARTESIAN_POINT('',(3.43,-4.20053852107542E-16,3.2));
#33446=CARTESIAN_POINT('Origin',(0.,0.,3.2));
#33447=CARTESIAN_POINT('',(1.666,2.04026156737949E-16,3.2));
#33448=CARTESIAN_POINT('Origin',(0.,0.,3.2));
#33449=CARTESIAN_POINT('Origin',(0.,0.,3.05719327969003));
#33450=CARTESIAN_POINT('',(3.73625,-4.5755866033143E-16,3.05719327969003));
#33451=CARTESIAN_POINT('Origin',(-2.,0.,-2.19122965386544E-16));
#33452=CARTESIAN_POINT('',(1.666,-2.04026156737949E-16,-2.77555756156289E-16));
#33453=CARTESIAN_POINT('Origin',(0.,0.,-2.77555756156289E-16));
#33454=CARTESIAN_POINT('Origin',(0.,0.,1.6));
#33455=CARTESIAN_POINT('',(1.666,-2.04026156737949E-16,1.6));
#33466=UNCERTAINTY_MEASURE_WITH_UNIT(LENGTH_MEASURE(0.01),#33475,
'DISTANCE_ACCURACY_VALUE',
'Maximum model space distance between geometric entities at asserted c
onnectivities');
#33467=UNCERTAINTY_MEASURE_WITH_UNIT(LENGTH_MEASURE(0.01),#33475,
'DISTANCE_ACCURACY_VALUE',
'Maximum model space distance between geometric entities at asserted c
onnectivities');
#33473=(
GEOMETRIC_REPRESENTATION_CONTEXT(3)
GLOBAL_UNCERTAINTY_ASSIGNED_CONTEXT((#33466))
GLOBAL_UNIT_ASSIGNED_CONTEXT((#33475,#33477,#33478))
REPRESENTATION_CONTEXT('','3D')
);
#33474=(
GEOMETRIC_REPRESENTATION_CONTEXT(3)
GLOBAL_UNCERTAINTY_ASSIGNED_CONTEXT((#33467))
GLOBAL_UNIT_ASSIGNED_CONTEXT((#33475,#33477,#33478))
REPRESENTATION_CONTEXT('','3D')
);
#33475=(
LENGTH_UNIT()
NAMED_UNIT(*)
SI_UNIT(.MILLI.,.METRE.)
);
#33477=(
NAMED_UNIT(*)
PLANE_ANGLE_UNIT()
SI_UNIT($,.RADIAN.)
);
#33478=(
NAMED_UNIT(*)
SI_UNIT($,.STERADIAN.)
SOLID_ANGLE_UNIT()
);
#33484=SHAPE_DEFINITION_REPRESENTATION(#33490,#33501);
#33490=PRODUCT_DEFINITION_SHAPE('',$,#33508);
#33501=SHAPE_REPRESENTATION('',(#3128),#33473);
#33502=PRODUCT_DEFINITION_CONTEXT('part definition',#33522,'design');
#33508=PRODUCT_DEFINITION('2026-10-04-16-34-53-963','Nut',#33514,#33502);
#33514=PRODUCT_DEFINITION_FORMATION('',$,#33529);
#33522=APPLICATION_CONTEXT(
'Core Data for Automotive Mechanical Design Process');
#33523=PRODUCT_CONTEXT('part definition',#33522,'mechanical');
#33529=PRODUCT('2026-10-04-16-34-53-963','Nut',
'Hex Nut Style 1 ASME B18.2.4.1M - M4',(#33523));
#33530=PRESENTATION_STYLE_ASSIGNMENT((#33532));
#33532=SURFACE_STYLE_USAGE(.BOTH.,#33534);
#33534=SURFACE_SIDE_STYLE('',(#33536));
#33536=SURFACE_STYLE_FILL_AREA(#33538);
#33538=FILL_AREA_STYLE('Steel - Satin',(#33540));
#33540=FILL_AREA_STYLE_COLOUR('Steel - Satin',#33542);
#33542=COLOUR_RGB('Steel - Satin', 0.72549020, 0.75294118, 0.79215686);
ENDSEC;
END-ISO-10303-21;
